ISO-10303-21;
HEADER;
/* Generated by software containing ST-Developer
 * from STEP Tools, Inc. (www.steptools.com) 
 */

FILE_DESCRIPTION(
/* description */ ('PAT-082'),
/* implementation_level */ '2;1');

FILE_NAME(
/* name */ 'Hex Pipe Nipple - 1-4 Inch Tapered Pipe Thread.step',
/* time_stamp */ '2026-10-29T20:16:13-07:00',
/* author */ (''),
/* organization */ (''),
/* preprocessor_version */ 'ST-DEVELOPER v20.2',
/* originating_system */ 'Autodesk Translation Framework v15.17.0.0',
/* authorisation */ '');

FILE_SCHEMA (('AUTOMOTIVE_DESIGN { 1 0 10303 214 3 1 1 }'));
ENDSEC;

DATA;
#10=MECHANICAL_DESIGN_GEOMETRIC_PRESENTATION_REPRESENTATION('',(#260),#8266);
#170=CONICAL_SURFACE('',#5287,0.645,0.785398163397448);
#171=CONICAL_SURFACE('',#5290,0.645,0.785398163397448);
#216=SHAPE_REPRESENTATION_RELATIONSHIP('SRR','None',#8379,#238);
#238=ADVANCED_BREP_SHAPE_REPRESENTATION('',(#281),#8263);
#260=STYLED_ITEM('',(#8530),#281);
#281=MANIFOLD_SOLID_BREP('Body1',#4601);
#399=FACE_BOUND('',#1182,.T.);
#400=FACE_BOUND('',#1184,.T.);
#401=FACE_BOUND('',#1193,.T.);
#402=FACE_BOUND('',#1198,.T.);
#540=PLANE('',#5272);
#541=PLANE('',#5274);
#542=PLANE('',#5276);
#543=PLANE('',#5277);
#544=PLANE('',#5278);
#545=PLANE('',#5279);
#546=PLANE('',#5280);
#547=PLANE('',#5281);
#548=PLANE('',#5284);
#549=PLANE('',#5292);
#794=FACE_OUTER_BOUND('',#1181,.T.);
#795=FACE_OUTER_BOUND('',#1183,.T.);
#796=FACE_OUTER_BOUND('',#1185,.T.);
#797=FACE_OUTER_BOUND('',#1186,.T.);
#798=FACE_OUTER_BOUND('',#1187,.T.);
#799=FACE_OUTER_BOUND('',#1188,.T.);
#800=FACE_OUTER_BOUND('',#1189,.T.);
#801=FACE_OUTER_BOUND('',#1190,.T.);
#802=FACE_OUTER_BOUND('',#1191,.T.);
#803=FACE_OUTER_BOUND('',#1192,.T.);
#804=FACE_OUTER_BOUND('',#1194,.T.);
#805=FACE_OUTER_BOUND('',#1195,.T.);
#806=FACE_OUTER_BOUND('',#1196,.T.);
#807=FACE_OUTER_BOUND('',#1197,.T.);
#808=FACE_OUTER_BOUND('',#1199,.T.);
#1181=EDGE_LOOP('',(#4034,#4035,#4036,#4037,#4038,#4039));
#1182=EDGE_LOOP('',(#4040));
#1183=EDGE_LOOP('',(#4041,#4042,#4043,#4044,#4045,#4046));
#1184=EDGE_LOOP('',(#4047));
#1185=EDGE_LOOP('',(#4048,#4049,#4050,#4051));
#1186=EDGE_LOOP('',(#4052,#4053,#4054,#4055));
#1187=EDGE_LOOP('',(#4056,#4057,#4058,#4059));
#1188=EDGE_LOOP('',(#4060,#4061,#4062,#4063));
#1189=EDGE_LOOP('',(#4064,#4065,#4066,#4067));
#1190=EDGE_LOOP('',(#4068,#4069,#4070,#4071));
#1191=EDGE_LOOP('',(#4072,#4073,#4074,#4075));
#1192=EDGE_LOOP('',(#4076));
#1193=EDGE_LOOP('',(#4077));
#1194=EDGE_LOOP('',(#4078,#4079,#4080,#4081));
#1195=EDGE_LOOP('',(#4082,#4083,#4084,#4085));
#1196=EDGE_LOOP('',(#4086,#4087,#4088,#4089));
#1197=EDGE_LOOP('',(#4090));
#1198=EDGE_LOOP('',(#4091));
#1199=EDGE_LOOP('',(#4092,#4093,#4094,#4095));
#1520=LINE('',#7981,#1875);
#1521=LINE('',#7983,#1876);
#1522=LINE('',#7985,#1877);
#1523=LINE('',#7987,#1878);
#1524=LINE('',#7989,#1879);
#1525=LINE('',#7990,#1880);
#1526=LINE('',#7996,#1881);
#1527=LINE('',#7998,#1882);
#1528=LINE('',#8000,#1883);
#1529=LINE('',#8002,#1884);
#1530=LINE('',#8004,#1885);
#1531=LINE('',#8005,#1886);
#1532=LINE('',#8009,#1887);
#1533=LINE('',#8010,#1888);
#1534=LINE('',#8012,#1889);
#1535=LINE('',#8014,#1890);
#1536=LINE('',#8016,#1891);
#1537=LINE('',#8018,#1892);
#1538=LINE('',#8022,#1893);
#1539=LINE('',#8030,#1894);
#1540=LINE('',#8034,#1895);
#1541=LINE('',#8038,#1896);
#1542=LINE('',#8043,#1897);
#1875=VECTOR('',#6515,1.);
#1876=VECTOR('',#6516,1.);
#1877=VECTOR('',#6517,1.);
#1878=VECTOR('',#6518,1.);
#1879=VECTOR('',#6519,1.);
#1880=VECTOR('',#6520,1.);
#1881=VECTOR('',#6525,1.);
#1882=VECTOR('',#6526,1.);
#1883=VECTOR('',#6527,1.);
#1884=VECTOR('',#6528,1.);
#1885=VECTOR('',#6529,1.);
#1886=VECTOR('',#6530,1.);
#1887=VECTOR('',#6535,1.);
#1888=VECTOR('',#6536,1.);
#1889=VECTOR('',#6539,1.);
#1890=VECTOR('',#6542,1.);
#1891=VECTOR('',#6545,1.);
#1892=VECTOR('',#6548,1.);
#1893=VECTOR('',#6553,0.685);
#1894=VECTOR('',#6564,0.645);
#1895=VECTOR('',#6569,0.685);
#1896=VECTOR('',#6574,0.645);
#1897=VECTOR('',#6581,0.46);
#2122=CIRCLE('',#5273,0.685);
#2123=CIRCLE('',#5275,0.685);
#2124=CIRCLE('',#5283,0.685);
#2125=CIRCLE('',#5285,0.605);
#2126=CIRCLE('',#5286,0.46);
#2127=CIRCLE('',#5289,0.685);
#2128=CIRCLE('',#5291,0.605);
#2129=CIRCLE('',#5293,0.46);
#2460=VERTEX_POINT('',#7979);
#2461=VERTEX_POINT('',#7980);
#2462=VERTEX_POINT('',#7982);
#2463=VERTEX_POINT('',#7984);
#2464=VERTEX_POINT('',#7986);
#2465=VERTEX_POINT('',#7988);
#2466=VERTEX_POINT('',#7991);
#2467=VERTEX_POINT('',#7994);
#2468=VERTEX_POINT('',#7995);
#2469=VERTEX_POINT('',#7997);
#2470=VERTEX_POINT('',#7999);
#2471=VERTEX_POINT('',#8001);
#2472=VERTEX_POINT('',#8003);
#2473=VERTEX_POINT('',#8006);
#2474=VERTEX_POINT('',#8021);
#2475=VERTEX_POINT('',#8025);
#2476=VERTEX_POINT('',#8027);
#2477=VERTEX_POINT('',#8032);
#2478=VERTEX_POINT('',#8036);
#2479=VERTEX_POINT('',#8040);
#2993=EDGE_CURVE('',#2460,#2461,#1520,.T.);
#2994=EDGE_CURVE('',#2461,#2462,#1521,.T.);
#2995=EDGE_CURVE('',#2462,#2463,#1522,.T.);
#2996=EDGE_CURVE('',#2463,#2464,#1523,.T.);
#2997=EDGE_CURVE('',#2464,#2465,#1524,.T.);
#2998=EDGE_CURVE('',#2465,#2460,#1525,.T.);
#2999=EDGE_CURVE('',#2466,#2466,#2122,.T.);
#3000=EDGE_CURVE('',#2467,#2468,#1526,.T.);
#3001=EDGE_CURVE('',#2468,#2469,#1527,.T.);
#3002=EDGE_CURVE('',#2469,#2470,#1528,.T.);
#3003=EDGE_CURVE('',#2470,#2471,#1529,.T.);
#3004=EDGE_CURVE('',#2471,#2472,#1530,.T.);
#3005=EDGE_CURVE('',#2472,#2467,#1531,.T.);
#3006=EDGE_CURVE('',#2473,#2473,#2123,.T.);
#3007=EDGE_CURVE('',#2467,#2461,#1532,.T.);
#3008=EDGE_CURVE('',#2462,#2472,#1533,.T.);
#3009=EDGE_CURVE('',#2463,#2471,#1534,.T.);
#3010=EDGE_CURVE('',#2464,#2470,#1535,.T.);
#3011=EDGE_CURVE('',#2465,#2469,#1536,.T.);
#3012=EDGE_CURVE('',#2460,#2468,#1537,.T.);
#3013=EDGE_CURVE('',#2473,#2474,#1538,.T.);
#3014=EDGE_CURVE('',#2474,#2474,#2124,.T.);
#3015=EDGE_CURVE('',#2475,#2475,#2125,.T.);
#3016=EDGE_CURVE('',#2476,#2476,#2126,.T.);
#3017=EDGE_CURVE('',#2474,#2475,#1539,.T.);
#3018=EDGE_CURVE('',#2477,#2477,#2127,.T.);
#3019=EDGE_CURVE('',#2477,#2466,#1540,.T.);
#3020=EDGE_CURVE('',#2478,#2478,#2128,.T.);
#3021=EDGE_CURVE('',#2478,#2477,#1541,.T.);
#3022=EDGE_CURVE('',#2479,#2479,#2129,.T.);
#3023=EDGE_CURVE('',#2479,#2476,#1542,.T.);
#4034=ORIENTED_EDGE('',*,*,#2993,.T.);
#4035=ORIENTED_EDGE('',*,*,#2994,.T.);
#4036=ORIENTED_EDGE('',*,*,#2995,.T.);
#4037=ORIENTED_EDGE('',*,*,#2996,.T.);
#4038=ORIENTED_EDGE('',*,*,#2997,.T.);
#4039=ORIENTED_EDGE('',*,*,#2998,.T.);
#4040=ORIENTED_EDGE('',*,*,#2999,.F.);
#4041=ORIENTED_EDGE('',*,*,#3000,.T.);
#4042=ORIENTED_EDGE('',*,*,#3001,.T.);
#4043=ORIENTED_EDGE('',*,*,#3002,.T.);
#4044=ORIENTED_EDGE('',*,*,#3003,.T.);
#4045=ORIENTED_EDGE('',*,*,#3004,.T.);
#4046=ORIENTED_EDGE('',*,*,#3005,.T.);
#4047=ORIENTED_EDGE('',*,*,#3006,.F.);
#4048=ORIENTED_EDGE('',*,*,#3007,.F.);
#4049=ORIENTED_EDGE('',*,*,#3005,.F.);
#4050=ORIENTED_EDGE('',*,*,#3008,.F.);
#4051=ORIENTED_EDGE('',*,*,#2994,.F.);
#4052=ORIENTED_EDGE('',*,*,#3008,.T.);
#4053=ORIENTED_EDGE('',*,*,#3004,.F.);
#4054=ORIENTED_EDGE('',*,*,#3009,.F.);
#4055=ORIENTED_EDGE('',*,*,#2995,.F.);
#4056=ORIENTED_EDGE('',*,*,#3009,.T.);
#4057=ORIENTED_EDGE('',*,*,#3003,.F.);
#4058=ORIENTED_EDGE('',*,*,#3010,.F.);
#4059=ORIENTED_EDGE('',*,*,#2996,.F.);
#4060=ORIENTED_EDGE('',*,*,#3010,.T.);
#4061=ORIENTED_EDGE('',*,*,#3002,.F.);
#4062=ORIENTED_EDGE('',*,*,#3011,.F.);
#4063=ORIENTED_EDGE('',*,*,#2997,.F.);
#4064=ORIENTED_EDGE('',*,*,#3011,.T.);
#4065=ORIENTED_EDGE('',*,*,#3001,.F.);
#4066=ORIENTED_EDGE('',*,*,#3012,.F.);
#4067=ORIENTED_EDGE('',*,*,#2998,.F.);
#4068=ORIENTED_EDGE('',*,*,#3012,.T.);
#4069=ORIENTED_EDGE('',*,*,#3000,.F.);
#4070=ORIENTED_EDGE('',*,*,#3007,.T.);
#4071=ORIENTED_EDGE('',*,*,#2993,.F.);
#4072=ORIENTED_EDGE('',*,*,#3006,.T.);
#4073=ORIENTED_EDGE('',*,*,#3013,.T.);
#4074=ORIENTED_EDGE('',*,*,#3014,.T.);
#4075=ORIENTED_EDGE('',*,*,#3013,.F.);
#4076=ORIENTED_EDGE('',*,*,#3015,.F.);
#4077=ORIENTED_EDGE('',*,*,#3016,.T.);
#4078=ORIENTED_EDGE('',*,*,#3014,.F.);
#4079=ORIENTED_EDGE('',*,*,#3017,.T.);
#4080=ORIENTED_EDGE('',*,*,#3015,.T.);
#4081=ORIENTED_EDGE('',*,*,#3017,.F.);
#4082=ORIENTED_EDGE('',*,*,#3018,.F.);
#4083=ORIENTED_EDGE('',*,*,#3019,.T.);
#4084=ORIENTED_EDGE('',*,*,#2999,.T.);
#4085=ORIENTED_EDGE('',*,*,#3019,.F.);
#4086=ORIENTED_EDGE('',*,*,#3020,.F.);
#4087=ORIENTED_EDGE('',*,*,#3021,.T.);
#4088=ORIENTED_EDGE('',*,*,#3018,.T.);
#4089=ORIENTED_EDGE('',*,*,#3021,.F.);
#4090=ORIENTED_EDGE('',*,*,#3020,.T.);
#4091=ORIENTED_EDGE('',*,*,#3022,.F.);
#4092=ORIENTED_EDGE('',*,*,#3022,.T.);
#4093=ORIENTED_EDGE('',*,*,#3023,.T.);
#4094=ORIENTED_EDGE('',*,*,#3016,.F.);
#4095=ORIENTED_EDGE('',*,*,#3023,.F.);
#4304=CYLINDRICAL_SURFACE('',#5282,0.685);
#4305=CYLINDRICAL_SURFACE('',#5288,0.685);
#4306=CYLINDRICAL_SURFACE('',#5294,0.46);
#4533=ADVANCED_FACE('',(#794,#399),#540,.F.);
#4534=ADVANCED_FACE('',(#795,#400),#541,.T.);
#4535=ADVANCED_FACE('',(#796),#542,.T.);
#4536=ADVANCED_FACE('',(#797),#543,.T.);
#4537=ADVANCED_FACE('',(#798),#544,.T.);
#4538=ADVANCED_FACE('',(#799),#545,.T.);
#4539=ADVANCED_FACE('',(#800),#546,.T.);
#4540=ADVANCED_FACE('',(#801),#547,.T.);
#4541=ADVANCED_FACE('',(#802),#4304,.T.);
#4542=ADVANCED_FACE('',(#803,#401),#548,.T.);
#4543=ADVANCED_FACE('',(#804),#170,.T.);
#4544=ADVANCED_FACE('',(#805),#4305,.T.);
#4545=ADVANCED_FACE('',(#806),#171,.T.);
#4546=ADVANCED_FACE('',(#807,#402),#549,.T.);
#4547=ADVANCED_FACE('',(#808),#4306,.F.);
#4601=CLOSED_SHELL('',(#4533,#4534,#4535,#4536,#4537,#4538,#4539,#4540,
#4541,#4542,#4543,#4544,#4545,#4546,#4547));
#5271=AXIS2_PLACEMENT_3D('',#7977,#6511,#6512);
#5272=AXIS2_PLACEMENT_3D('',#7978,#6513,#6514);
#5273=AXIS2_PLACEMENT_3D('',#7992,#6521,#6522);
#5274=AXIS2_PLACEMENT_3D('',#7993,#6523,#6524);
#5275=AXIS2_PLACEMENT_3D('',#8007,#6531,#6532);
#5276=AXIS2_PLACEMENT_3D('',#8008,#6533,#6534);
#5277=AXIS2_PLACEMENT_3D('',#8011,#6537,#6538);
#5278=AXIS2_PLACEMENT_3D('',#8013,#6540,#6541);
#5279=AXIS2_PLACEMENT_3D('',#8015,#6543,#6544);
#5280=AXIS2_PLACEMENT_3D('',#8017,#6546,#6547);
#5281=AXIS2_PLACEMENT_3D('',#8019,#6549,#6550);
#5282=AXIS2_PLACEMENT_3D('',#8020,#6551,#6552);
#5283=AXIS2_PLACEMENT_3D('',#8023,#6554,#6555);
#5284=AXIS2_PLACEMENT_3D('',#8024,#6556,#6557);
#5285=AXIS2_PLACEMENT_3D('',#8026,#6558,#6559);
#5286=AXIS2_PLACEMENT_3D('',#8028,#6560,#6561);
#5287=AXIS2_PLACEMENT_3D('',#8029,#6562,#6563);
#5288=AXIS2_PLACEMENT_3D('',#8031,#6565,#6566);
#5289=AXIS2_PLACEMENT_3D('',#8033,#6567,#6568);
#5290=AXIS2_PLACEMENT_3D('',#8035,#6570,#6571);
#5291=AXIS2_PLACEMENT_3D('',#8037,#6572,#6573);
#5292=AXIS2_PLACEMENT_3D('',#8039,#6575,#6576);
#5293=AXIS2_PLACEMENT_3D('',#8041,#6577,#6578);
#5294=AXIS2_PLACEMENT_3D('',#8042,#6579,#6580);
#6511=DIRECTION('axis',(0.,0.,1.));
#6512=DIRECTION('refdir',(1.,0.,0.));
#6513=DIRECTION('center_axis',(0.,1.,0.));
#6514=DIRECTION('ref_axis',(1.,0.,0.));
#6515=DIRECTION('',(-0.5,0.,0.866025403784439));
#6516=DIRECTION('',(-1.,0.,-3.29650746237182E-16));
#6517=DIRECTION('',(-0.5,0.,-0.866025403784439));
#6518=DIRECTION('',(0.5,0.,-0.866025403784438));
#6519=DIRECTION('',(1.,0.,0.));
#6520=DIRECTION('',(0.5,0.,0.866025403784439));
#6521=DIRECTION('center_axis',(0.,-1.,0.));
#6522=DIRECTION('ref_axis',(1.,0.,0.));
#6523=DIRECTION('center_axis',(0.,1.,0.));
#6524=DIRECTION('ref_axis',(1.,0.,0.));
#6525=DIRECTION('',(0.5,0.,-0.866025403784439));
#6526=DIRECTION('',(-0.5,0.,-0.866025403784439));
#6527=DIRECTION('',(-1.,0.,0.));
#6528=DIRECTION('',(-0.5,0.,0.866025403784438));
#6529=DIRECTION('',(0.5,0.,0.866025403784439));
#6530=DIRECTION('',(1.,0.,3.29650746237182E-16));
#6531=DIRECTION('center_axis',(0.,1.,0.));
#6532=DIRECTION('ref_axis',(1.,0.,0.));
#6533=DIRECTION('center_axis',(-3.29650746237182E-16,0.,1.));
#6534=DIRECTION('ref_axis',(1.,0.,3.29650746237182E-16));
#6535=DIRECTION('',(0.,-1.,0.));
#6536=DIRECTION('',(0.,1.,0.));
#6537=DIRECTION('center_axis',(-0.866025403784439,0.,0.5));
#6538=DIRECTION('ref_axis',(0.5,0.,0.866025403784439));
#6539=DIRECTION('',(0.,1.,0.));
#6540=DIRECTION('center_axis',(-0.866025403784439,0.,-0.5));
#6541=DIRECTION('ref_axis',(-0.5,0.,0.866025403784439));
#6542=DIRECTION('',(0.,1.,0.));
#6543=DIRECTION('center_axis',(0.,0.,-1.));
#6544=DIRECTION('ref_axis',(-1.,0.,0.));
#6545=DIRECTION('',(0.,1.,0.));
#6546=DIRECTION('center_axis',(0.866025403784439,0.,-0.5));
#6547=DIRECTION('ref_axis',(-0.5,0.,-0.866025403784439));
#6548=DIRECTION('',(0.,1.,0.));
#6549=DIRECTION('center_axis',(0.866025403784439,0.,0.5));
#6550=DIRECTION('ref_axis',(0.5,0.,-0.866025403784439));
#6551=DIRECTION('center_axis',(0.,-1.,0.));
#6552=DIRECTION('ref_axis',(1.,0.,0.));
#6553=DIRECTION('',(0.,1.,0.));
#6554=DIRECTION('center_axis',(0.,-1.,0.));
#6555=DIRECTION('ref_axis',(1.,0.,0.));
#6556=DIRECTION('center_axis',(0.,1.,0.));
#6557=DIRECTION('ref_axis',(0.,0.,1.));
#6558=DIRECTION('center_axis',(0.,-1.,0.));
#6559=DIRECTION('ref_axis',(1.,0.,0.));
#6560=DIRECTION('center_axis',(0.,-1.,0.));
#6561=DIRECTION('ref_axis',(1.,0.,0.));
#6562=DIRECTION('center_axis',(0.,-1.,0.));
#6563=DIRECTION('ref_axis',(1.,0.,0.));
#6564=DIRECTION('',(0.707106781186547,0.707106781186548,8.65956056235493E-17));
#6565=DIRECTION('center_axis',(0.,-1.,0.));
#6566=DIRECTION('ref_axis',(1.,0.,0.));
#6567=DIRECTION('center_axis',(0.,-1.,0.));
#6568=DIRECTION('ref_axis',(1.,0.,0.));
#6569=DIRECTION('',(0.,1.,0.));
#6570=DIRECTION('center_axis',(0.,1.,0.));
#6571=DIRECTION('ref_axis',(1.,0.,0.));
#6572=DIRECTION('center_axis',(0.,-1.,0.));
#6573=DIRECTION('ref_axis',(1.,0.,0.));
#6574=DIRECTION('',(-0.707106781186547,0.707106781186548,-8.65956056235493E-17));
#6575=DIRECTION('center_axis',(0.,-1.,0.));
#6576=DIRECTION('ref_axis',(0.,0.,-1.));
#6577=DIRECTION('center_axis',(0.,-1.,0.));
#6578=DIRECTION('ref_axis',(1.,0.,0.));
#6579=DIRECTION('center_axis',(0.,-1.,0.));
#6580=DIRECTION('ref_axis',(1.,0.,0.));
#6581=DIRECTION('',(0.,1.,0.));
#7977=CARTESIAN_POINT('',(0.,0.,0.));
#7978=CARTESIAN_POINT('Origin',(0.,-0.4,0.));
#7979=CARTESIAN_POINT('',(1.01036297108185,-0.4,0.));
#7980=CARTESIAN_POINT('',(0.505181485540923,-0.4,0.875));
#7981=CARTESIAN_POINT('',(0.505181485540923,-0.4,0.875));
#7982=CARTESIAN_POINT('',(-0.505181485540923,-0.4,0.875));
#7983=CARTESIAN_POINT('',(-0.505181485540923,-0.4,0.875));
#7984=CARTESIAN_POINT('',(-1.01036297108185,-0.4,-1.23733777851239E-16));
#7985=CARTESIAN_POINT('',(-1.01036297108185,-0.4,-1.23733777851239E-16));
#7986=CARTESIAN_POINT('',(-0.505181485540922,-0.4,-0.875));
#7987=CARTESIAN_POINT('',(-0.505181485540922,-0.4,-0.875));
#7988=CARTESIAN_POINT('',(0.505181485540923,-0.4,-0.875));
#7989=CARTESIAN_POINT('',(0.505181485540923,-0.4,-0.875));
#7990=CARTESIAN_POINT('',(1.01036297108185,-0.4,0.));
#7991=CARTESIAN_POINT('',(-0.685,-0.4,-8.38883057415937E-17));
#7992=CARTESIAN_POINT('Origin',(0.,-0.4,0.));
#7993=CARTESIAN_POINT('Origin',(0.,0.4,0.));
#7994=CARTESIAN_POINT('',(0.505181485540923,0.4,0.875));
#7995=CARTESIAN_POINT('',(1.01036297108185,0.4,0.));
#7996=CARTESIAN_POINT('',(0.505181485540923,0.4,0.875));
#7997=CARTESIAN_POINT('',(0.505181485540923,0.4,-0.875));
#7998=CARTESIAN_POINT('',(1.01036297108185,0.4,0.));
#7999=CARTESIAN_POINT('',(-0.505181485540922,0.4,-0.875));
#8000=CARTESIAN_POINT('',(0.505181485540923,0.4,-0.875));
#8001=CARTESIAN_POINT('',(-1.01036297108185,0.4,-1.23733777851239E-16));
#8002=CARTESIAN_POINT('',(-0.505181485540922,0.4,-0.875));
#8003=CARTESIAN_POINT('',(-0.505181485540923,0.4,0.875));
#8004=CARTESIAN_POINT('',(-1.01036297108185,0.4,-1.23733777851239E-16));
#8005=CARTESIAN_POINT('',(-0.505181485540923,0.4,0.875));
#8006=CARTESIAN_POINT('',(-0.685,0.4,8.38883057415937E-17));
#8007=CARTESIAN_POINT('Origin',(0.,0.4,0.));
#8008=CARTESIAN_POINT('Origin',(-0.505181485540923,0.,0.875));
#8009=CARTESIAN_POINT('',(0.505181485540923,0.,0.875));
#8010=CARTESIAN_POINT('',(-0.505181485540923,0.,0.875));
#8011=CARTESIAN_POINT('Origin',(-1.01036297108185,0.,-1.23733777851239E-16));
#8012=CARTESIAN_POINT('',(-1.01036297108185,0.,-1.23733777851239E-16));
#8013=CARTESIAN_POINT('Origin',(-0.505181485540922,0.,-0.875));
#8014=CARTESIAN_POINT('',(-0.505181485540922,0.,-0.875));
#8015=CARTESIAN_POINT('Origin',(0.505181485540923,0.,-0.875));
#8016=CARTESIAN_POINT('',(0.505181485540923,0.,-0.875));
#8017=CARTESIAN_POINT('Origin',(1.01036297108185,0.,0.));
#8018=CARTESIAN_POINT('',(1.01036297108185,0.,0.));
#8019=CARTESIAN_POINT('Origin',(0.505181485540923,0.,0.875));
#8020=CARTESIAN_POINT('Origin',(0.,0.,0.));
#8021=CARTESIAN_POINT('',(-0.685,1.82,-8.38883057415937E-17));
#8022=CARTESIAN_POINT('',(-0.685,0.,-8.38883057415937E-17));
#8023=CARTESIAN_POINT('Origin',(0.,1.82,0.));
#8024=CARTESIAN_POINT('Origin',(0.605,1.9,0.));
#8025=CARTESIAN_POINT('',(-0.605,1.9,-7.40911313484149E-17));
#8026=CARTESIAN_POINT('Origin',(0.,1.9,0.));
#8027=CARTESIAN_POINT('',(-0.46,1.9,-5.63337527607782E-17));
#8028=CARTESIAN_POINT('Origin',(0.,1.9,0.));
#8029=CARTESIAN_POINT('Origin',(0.,1.86,0.));
#8030=CARTESIAN_POINT('',(-0.645,1.86,-7.89897185450043E-17));
#8031=CARTESIAN_POINT('Origin',(0.,0.,0.));
#8032=CARTESIAN_POINT('',(-0.685,-1.82,-8.38883057415937E-17));
#8033=CARTESIAN_POINT('Origin',(0.,-1.82,0.));
#8034=CARTESIAN_POINT('',(-0.685,0.,-8.38883057415937E-17));
#8035=CARTESIAN_POINT('Origin',(0.,-1.86,0.));
#8036=CARTESIAN_POINT('',(-0.605,-1.9,-7.40911313484149E-17));
#8037=CARTESIAN_POINT('Origin',(0.,-1.9,0.));
#8038=CARTESIAN_POINT('',(-0.645,-1.86,-7.89897185450043E-17));
#8039=CARTESIAN_POINT('Origin',(0.46,-1.9,0.));
#8040=CARTESIAN_POINT('',(-0.46,-1.9,-5.63337527607782E-17));
#8041=CARTESIAN_POINT('Origin',(0.,-1.9,0.));
#8042=CARTESIAN_POINT('Origin',(0.,0.,0.));
#8043=CARTESIAN_POINT('',(-0.46,0.,-5.63337527607782E-17));
#8238=UNCERTAINTY_MEASURE_WITH_UNIT(LENGTH_MEASURE(0.001),#8267,
'DISTANCE_ACCURACY_VALUE',
'Maximum model space distance between geometric entities at asserted c
onnectivities');
#8241=UNCERTAINTY_MEASURE_WITH_UNIT(LENGTH_MEASURE(0.001),#8267,
'DISTANCE_ACCURACY_VALUE',
'Maximum model space distance between geometric entities at asserted c
onnectivities');
#8263=(
GEOMETRIC_REPRESENTATION_CONTEXT(3)
GLOBAL_UNCERTAINTY_ASSIGNED_CONTEXT((#8238))
GLOBAL_UNIT_ASSIGNED_CONTEXT((#8267,#8269,#8270))
REPRESENTATION_CONTEXT('','3D')
);
#8266=(
GEOMETRIC_REPRESENTATION_CONTEXT(3)
GLOBAL_UNCERTAINTY_ASSIGNED_CONTEXT((#8241))
GLOBAL_UNIT_ASSIGNED_CONTEXT((#8267,#8269,#8270))
REPRESENTATION_CONTEXT('','3D')
);
#8267=(
LENGTH_UNIT()
NAMED_UNIT(*)
SI_UNIT(.CENTI.,.METRE.)
);
#8269=(
NAMED_UNIT(*)
PLANE_ANGLE_UNIT()
SI_UNIT($,.RADIAN.)
);
#8270=(
NAMED_UNIT(*)
SI_UNIT($,.STERADIAN.)
SOLID_ANGLE_UNIT()
);
#8292=SHAPE_DEFINITION_REPRESENTATION(#8318,#8379);
#8318=PRODUCT_DEFINITION_SHAPE('',$,#8404);
#8379=SHAPE_REPRESENTATION('',(#5271),#8263);
#8382=PRODUCT_DEFINITION_CONTEXT('part definition',#8456,'design');
#8404=PRODUCT_DEFINITION('Hex Pipe Nipple - 1-4 Inch Tapered Pipe Thread',
'Hex Pipe Nipple - 1-4 Inch Tapered Pipe Thread',#8428,#8382);
#8428=PRODUCT_DEFINITION_FORMATION('',$,#8479);
#8456=APPLICATION_CONTEXT(
'Core Data for Automotive Mechanical Design Process');
#8457=PRODUCT_CONTEXT('part definition',#8456,'mechanical');
#8479=PRODUCT('Hex Pipe Nipple - 1-4 Inch Tapered Pipe Thread',
'Hex Pipe Nipple - 1-4 Inch Tapered Pipe Thread',
'Hex Pipe Nipple - 1-4 Inch Tapered Pipe Thread',(#8457));
#8524=COLOUR_RGB('Sky Blue',0.24,0.69,0.87);
#8525=FILL_AREA_STYLE_COLOUR('',#8524);
#8526=FILL_AREA_STYLE('',(#8525));
#8527=SURFACE_STYLE_FILL_AREA(#8526);
#8528=SURFACE_SIDE_STYLE('',(#8527));
#8529=SURFACE_STYLE_USAGE(.BOTH.,#8528);
#8530=PRESENTATION_STYLE_ASSIGNMENT((#8529));
ENDSEC;
END-ISO-10303-21;
